ISO-10303-21;
HEADER;
/* Generated by software containing ST-Developer
 * from STEP Tools, Inc. (www.steptools.com) 
 */
/* OPTION: using custom renumber hook */

FILE_DESCRIPTION(
/* description */ ('STEP AP242 Edition 2', 'CAx-IF Rec.Pracs.---Representation and Presentation of Product Manufa
cturing Information (PMI)---4.0---2014-10-13', 'CAx-IF Rec.Pracs.---3D Tessellated Geometry---0.4---2014-09-14', '2;1', 'CAx-IF Rec.Pracs.---User Defined Attributes---1.5---2016-08-15'),
/* implementation_level */ '2;1');

FILE_NAME(
/* name */ 'Part 2.step',
/* time_stamp */ '2026-10-09T13:59:33Z',
/* author */ (''),
/* organization */ (''),
/* preprocessor_version */ 'ST-DEVELOPER v20',
/* originating_system */ 'ONSHAPE BY PTC INC, 1.221',
/* authorisation */ '  ');

FILE_SCHEMA (('AP242_MANAGED_MODEL_BASED_3D_ENGINEERING_MIM_LF { 1 0 10303 442 3 1 4 }'));
ENDSEC;

DATA;
#172=LINE('',#9155,#456);
#173=LINE('',#9158,#457);
#174=LINE('',#9160,#458);
#175=LINE('',#9162,#459);
#176=LINE('',#9164,#460);
#177=LINE('',#9166,#461);
#178=LINE('',#9168,#462);
#179=LINE('',#9170,#463);
#180=LINE('',#9172,#464);
#181=LINE('',#9174,#465);
#182=LINE('',#9181,#466);
#183=LINE('',#9182,#467);
#456=VECTOR('',#7304,1.);
#457=VECTOR('',#7305,1.);
#458=VECTOR('',#7306,1.);
#459=VECTOR('',#7307,1.);
#460=VECTOR('',#7310,1.);
#461=VECTOR('',#7311,1.);
#462=VECTOR('',#7312,1.);
#463=VECTOR('',#7315,1.);
#464=VECTOR('',#7316,1.);
#465=VECTOR('',#7317,1.);
#466=VECTOR('',#7326,1.);
#467=VECTOR('',#7327,1.);
#676=SHAPE_REPRESENTATION_RELATIONSHIP('','',#5694,#690);
#690=ADVANCED_BREP_SHAPE_REPRESENTATION('',(#5663),#10148);
#749=PLANE('',#6034);
#750=PLANE('',#6035);
#751=PLANE('',#6036);
#752=PLANE('',#6040);
#753=PLANE('',#6053);
#754=PLANE('',#6055);
#1476=ORIENTED_EDGE('',*,*,#2675,.F.);
#1477=ORIENTED_EDGE('',*,*,#2676,.F.);
#1478=ORIENTED_EDGE('',*,*,#2677,.T.);
#1479=ORIENTED_EDGE('',*,*,#2678,.T.);
#1480=ORIENTED_EDGE('',*,*,#2679,.T.);
#1481=ORIENTED_EDGE('',*,*,#2680,.F.);
#1482=ORIENTED_EDGE('',*,*,#2681,.F.);
#1483=ORIENTED_EDGE('',*,*,#2676,.T.);
#1484=ORIENTED_EDGE('',*,*,#2682,.T.);
#1485=ORIENTED_EDGE('',*,*,#2683,.F.);
#1486=ORIENTED_EDGE('',*,*,#2684,.F.);
#1487=ORIENTED_EDGE('',*,*,#2680,.T.);
#1488=ORIENTED_EDGE('',*,*,#2685,.F.);
#1489=ORIENTED_EDGE('',*,*,#2686,.T.);
#1490=ORIENTED_EDGE('',*,*,#2687,.F.);
#1491=ORIENTED_EDGE('',*,*,#2678,.F.);
#1492=ORIENTED_EDGE('',*,*,#2688,.T.);
#1493=ORIENTED_EDGE('',*,*,#2683,.T.);
#1494=ORIENTED_EDGE('',*,*,#2689,.F.);
#1495=ORIENTED_EDGE('',*,*,#2690,.T.);
#1496=ORIENTED_EDGE('',*,*,#2691,.F.);
#1497=ORIENTED_EDGE('',*,*,#2692,.T.);
#1498=ORIENTED_EDGE('',*,*,#2693,.T.);
#1499=ORIENTED_EDGE('',*,*,#2694,.F.);
#1500=ORIENTED_EDGE('',*,*,#2695,.T.);
#1501=ORIENTED_EDGE('',*,*,#2696,.F.);
#1502=ORIENTED_EDGE('',*,*,#2697,.T.);
#1503=ORIENTED_EDGE('',*,*,#2693,.F.);
#1504=ORIENTED_EDGE('',*,*,#2691,.T.);
#1505=ORIENTED_EDGE('',*,*,#2689,.T.);
#1506=ORIENTED_EDGE('',*,*,#2677,.F.);
#1507=ORIENTED_EDGE('',*,*,#2681,.T.);
#1508=ORIENTED_EDGE('',*,*,#2684,.T.);
#1509=ORIENTED_EDGE('',*,*,#2688,.F.);
#1510=ORIENTED_EDGE('',*,*,#2685,.T.);
#1511=ORIENTED_EDGE('',*,*,#2695,.F.);
#1512=ORIENTED_EDGE('',*,*,#2698,.F.);
#1513=ORIENTED_EDGE('',*,*,#2694,.T.);
#1514=ORIENTED_EDGE('',*,*,#2692,.F.);
#1515=ORIENTED_EDGE('',*,*,#2690,.F.);
#1516=ORIENTED_EDGE('',*,*,#2675,.T.);
#1517=ORIENTED_EDGE('',*,*,#2687,.T.);
#1518=ORIENTED_EDGE('',*,*,#2682,.F.);
#1519=ORIENTED_EDGE('',*,*,#2679,.F.);
#1520=ORIENTED_EDGE('',*,*,#2686,.F.);
#1521=ORIENTED_EDGE('',*,*,#2696,.T.);
#1522=ORIENTED_EDGE('',*,*,#2698,.T.);
#1523=ORIENTED_EDGE('',*,*,#2697,.F.);
#2675=EDGE_CURVE('',#3341,#3342,#172,.T.);
#2676=EDGE_CURVE('',#3343,#3341,#173,.T.);
#2677=EDGE_CURVE('',#3343,#3344,#174,.T.);
#2678=EDGE_CURVE('',#3344,#3342,#175,.T.);
#2679=EDGE_CURVE('',#3341,#3345,#176,.T.);
#2680=EDGE_CURVE('',#3346,#3345,#177,.T.);
#2681=EDGE_CURVE('',#3343,#3346,#178,.T.);
#2682=EDGE_CURVE('',#3345,#3347,#179,.T.);
#2683=EDGE_CURVE('',#3348,#3347,#180,.T.);
#2684=EDGE_CURVE('',#3346,#3348,#181,.T.);
#2685=EDGE_CURVE('',#3349,#3349,#3832,.T.);
#2686=EDGE_CURVE('',#3350,#3350,#3833,.T.);
#2687=EDGE_CURVE('',#3342,#3347,#182,.T.);
#2688=EDGE_CURVE('',#3344,#3348,#183,.T.);
#2689=EDGE_CURVE('',#3351,#3351,#3834,.T.);
#2690=EDGE_CURVE('',#3352,#3352,#3835,.T.);
#2691=EDGE_CURVE('',#3353,#3353,#3836,.T.);
#2692=EDGE_CURVE('',#3354,#3354,#3837,.T.);
#2693=EDGE_CURVE('',#3355,#3355,#3838,.F.);
#2694=EDGE_CURVE('',#3356,#3356,#3839,.F.);
#2695=EDGE_CURVE('',#3357,#3357,#3840,.F.);
#2696=EDGE_CURVE('',#3358,#3358,#3841,.F.);
#2697=EDGE_CURVE('',#3359,#3359,#3842,.T.);
#2698=EDGE_CURVE('',#3360,#3360,#3843,.T.);
#3341=VERTEX_POINT('',#9156);
#3342=VERTEX_POINT('',#9157);
#3343=VERTEX_POINT('',#9159);
#3344=VERTEX_POINT('',#9161);
#3345=VERTEX_POINT('',#9165);
#3346=VERTEX_POINT('',#9167);
#3347=VERTEX_POINT('',#9171);
#3348=VERTEX_POINT('',#9173);
#3349=VERTEX_POINT('',#9177);
#3350=VERTEX_POINT('',#9179);
#3351=VERTEX_POINT('',#9185);
#3352=VERTEX_POINT('',#9187);
#3353=VERTEX_POINT('',#9190);
#3354=VERTEX_POINT('',#9192);
#3355=VERTEX_POINT('',#9195);
#3356=VERTEX_POINT('',#9197);
#3357=VERTEX_POINT('',#9200);
#3358=VERTEX_POINT('',#9202);
#3359=VERTEX_POINT('',#9205);
#3360=VERTEX_POINT('',#9208);
#3832=CIRCLE('',#6038,0.0015);
#3833=CIRCLE('',#6039,0.0015);
#3834=CIRCLE('',#6042,0.0015);
#3835=CIRCLE('',#6043,0.0015);
#3836=CIRCLE('',#6045,0.0015);
#3837=CIRCLE('',#6046,0.0015);
#3838=CIRCLE('',#6048,0.0015);
#3839=CIRCLE('',#6049,0.0015);
#3840=CIRCLE('',#6051,0.0015);
#3841=CIRCLE('',#6052,0.0015);
#3842=CIRCLE('',#6054,0.0015);
#3843=CIRCLE('',#6056,0.0015);
#4296=EDGE_LOOP('',(#1476,#1477,#1478,#1479));
#4297=EDGE_LOOP('',(#1480,#1481,#1482,#1483));
#4298=EDGE_LOOP('',(#1484,#1485,#1486,#1487));
#4299=EDGE_LOOP('',(#1488));
#4300=EDGE_LOOP('',(#1489));
#4301=EDGE_LOOP('',(#1490,#1491,#1492,#1493));
#4302=EDGE_LOOP('',(#1494));
#4303=EDGE_LOOP('',(#1495));
#4304=EDGE_LOOP('',(#1496));
#4305=EDGE_LOOP('',(#1497));
#4306=EDGE_LOOP('',(#1498));
#4307=EDGE_LOOP('',(#1499));
#4308=EDGE_LOOP('',(#1500));
#4309=EDGE_LOOP('',(#1501));
#4310=EDGE_LOOP('',(#1502));
#4311=EDGE_LOOP('',(#1503));
#4312=EDGE_LOOP('',(#1504));
#4313=EDGE_LOOP('',(#1505));
#4314=EDGE_LOOP('',(#1506,#1507,#1508,#1509));
#4315=EDGE_LOOP('',(#1510));
#4316=EDGE_LOOP('',(#1511));
#4317=EDGE_LOOP('',(#1512));
#4318=EDGE_LOOP('',(#1513));
#4319=EDGE_LOOP('',(#1514));
#4320=EDGE_LOOP('',(#1515));
#4321=EDGE_LOOP('',(#1516,#1517,#1518,#1519));
#4322=EDGE_LOOP('',(#1520));
#4323=EDGE_LOOP('',(#1521));
#4324=EDGE_LOOP('',(#1522));
#4325=EDGE_LOOP('',(#1523));
#4744=FACE_BOUND('',#4296,.T.);
#4745=FACE_BOUND('',#4297,.T.);
#4746=FACE_BOUND('',#4298,.T.);
#4747=FACE_BOUND('',#4299,.T.);
#4748=FACE_BOUND('',#4300,.T.);
#4749=FACE_BOUND('',#4301,.T.);
#4750=FACE_BOUND('',#4302,.T.);
#4751=FACE_BOUND('',#4303,.T.);
#4752=FACE_BOUND('',#4304,.T.);
#4753=FACE_BOUND('',#4305,.T.);
#4754=FACE_BOUND('',#4306,.T.);
#4755=FACE_BOUND('',#4307,.T.);
#4756=FACE_BOUND('',#4308,.T.);
#4757=FACE_BOUND('',#4309,.T.);
#4758=FACE_BOUND('',#4310,.T.);
#4759=FACE_BOUND('',#4311,.T.);
#4760=FACE_BOUND('',#4312,.T.);
#4761=FACE_BOUND('',#4313,.T.);
#4762=FACE_BOUND('',#4314,.T.);
#4763=FACE_BOUND('',#4315,.T.);
#4764=FACE_BOUND('',#4316,.T.);
#4765=FACE_BOUND('',#4317,.T.);
#4766=FACE_BOUND('',#4318,.T.);
#4767=FACE_BOUND('',#4319,.T.);
#4768=FACE_BOUND('',#4320,.T.);
#4769=FACE_BOUND('',#4321,.T.);
#4770=FACE_BOUND('',#4322,.T.);
#4771=FACE_BOUND('',#4323,.T.);
#4772=FACE_BOUND('',#4324,.T.);
#4773=FACE_BOUND('',#4325,.T.);
#5086=CYLINDRICAL_SURFACE('',#6037,0.0015);
#5087=CYLINDRICAL_SURFACE('',#6041,0.0015);
#5088=CYLINDRICAL_SURFACE('',#6044,0.0015);
#5089=CYLINDRICAL_SURFACE('',#6047,0.0015);
#5090=CYLINDRICAL_SURFACE('',#6050,0.0015);
#5091=CYLINDRICAL_SURFACE('',#6057,0.0015);
#5353=ADVANCED_FACE('',(#4744),#749,.T.);
#5354=ADVANCED_FACE('',(#4745),#750,.F.);
#5355=ADVANCED_FACE('',(#4746),#751,.F.);
#5356=ADVANCED_FACE('',(#4747,#4748),#5086,.F.);
#5357=ADVANCED_FACE('',(#4749),#752,.T.);
#5358=ADVANCED_FACE('',(#4750,#4751),#5087,.F.);
#5359=ADVANCED_FACE('',(#4752,#4753),#5088,.F.);
#5360=ADVANCED_FACE('',(#4754,#4755),#5089,.F.);
#5361=ADVANCED_FACE('',(#4756,#4757),#5090,.F.);
#5362=ADVANCED_FACE('',(#4758,#4759,#4760,#4761,#4762,#4763,#4764),#753,
 .F.);
#5363=ADVANCED_FACE('',(#4765,#4766,#4767,#4768,#4769,#4770,#4771),#754,
 .T.);
#5364=ADVANCED_FACE('',(#4772,#4773),#5091,.F.);
#5544=CLOSED_SHELL('',(#5353,#5354,#5355,#5356,#5357,#5358,#5359,#5360,
#5361,#5362,#5363,#5364));
#5558=STYLED_ITEM('',(#5572),#5663);
#5572=PRESENTATION_STYLE_ASSIGNMENT((#5586));
#5586=SURFACE_STYLE_USAGE(.BOTH.,#5600);
#5600=SURFACE_SIDE_STYLE('',(#5614));
#5614=SURFACE_STYLE_FILL_AREA(#5628);
#5628=FILL_AREA_STYLE('',(#5642));
#5642=FILL_AREA_STYLE_COLOUR('',#5653);
#5653=COLOUR_RGB('', 0.40784314, 0.44705882, 0.49803922);
#5663=MANIFOLD_SOLID_BREP('Part 2',#5544);
#5678=SHAPE_DEFINITION_REPRESENTATION(#10190,#5694);
#5694=SHAPE_REPRESENTATION('Part 2',(#5704),#10148);
#5704=AXIS2_PLACEMENT_3D('',#8391,#6505,#6506);
#6034=AXIS2_PLACEMENT_3D('',#9154,#7302,#7303);
#6035=AXIS2_PLACEMENT_3D('',#9163,#7308,#7309);
#6036=AXIS2_PLACEMENT_3D('',#9169,#7313,#7314);
#6037=AXIS2_PLACEMENT_3D('',#9175,#7318,#7319);
#6038=AXIS2_PLACEMENT_3D('',#9176,#7320,#7321);
#6039=AXIS2_PLACEMENT_3D('',#9178,#7322,#7323);
#6040=AXIS2_PLACEMENT_3D('',#9180,#7324,#7325);
#6041=AXIS2_PLACEMENT_3D('',#9183,#7328,#7329);
#6042=AXIS2_PLACEMENT_3D('',#9184,#7330,#7331);
#6043=AXIS2_PLACEMENT_3D('',#9186,#7332,#7333);
#6044=AXIS2_PLACEMENT_3D('',#9188,#7334,#7335);
#6045=AXIS2_PLACEMENT_3D('',#9189,#7336,#7337);
#6046=AXIS2_PLACEMENT_3D('',#9191,#7338,#7339);
#6047=AXIS2_PLACEMENT_3D('',#9193,#7340,#7341);
#6048=AXIS2_PLACEMENT_3D('',#9194,#7342,#7343);
#6049=AXIS2_PLACEMENT_3D('',#9196,#7344,#7345);
#6050=AXIS2_PLACEMENT_3D('',#9198,#7346,#7347);
#6051=AXIS2_PLACEMENT_3D('',#9199,#7348,#7349);
#6052=AXIS2_PLACEMENT_3D('',#9201,#7350,#7351);
#6053=AXIS2_PLACEMENT_3D('',#9203,#7352,#7353);
#6054=AXIS2_PLACEMENT_3D('',#9204,#7354,#7355);
#6055=AXIS2_PLACEMENT_3D('',#9206,#7356,#7357);
#6056=AXIS2_PLACEMENT_3D('',#9207,#7358,#7359);
#6057=AXIS2_PLACEMENT_3D('',#9209,#7360,#7361);
#6505=DIRECTION('',(0.,0.,1.));
#6506=DIRECTION('',(1.,0.,0.));
#7302=DIRECTION('',(-0.866025403784439,0.,-0.5));
#7303=DIRECTION('',(-0.5,0.,0.866025403784439));
#7304=DIRECTION('',(0.5,0.,-0.866025403784439));
#7305=DIRECTION('',(0.,-1.,0.));
#7306=DIRECTION('',(0.5,0.,-0.866025403784439));
#7307=DIRECTION('',(0.,-1.,0.));
#7308=DIRECTION('',(0.5,0.,-0.866025403784439));
#7309=DIRECTION('',(-0.866025403784439,0.,-0.5));
#7310=DIRECTION('',(0.866025403784439,0.,0.5));
#7311=DIRECTION('',(0.,-1.,0.));
#7312=DIRECTION('',(0.866025403784439,0.,0.5));
#7313=DIRECTION('',(-0.866025403784434,0.,-0.500000000000008));
#7314=DIRECTION('',(-0.500000000000009,0.,0.866025403784434));
#7315=DIRECTION('',(0.500000000000009,0.,-0.866025403784434));
#7316=DIRECTION('',(0.,-1.,0.));
#7317=DIRECTION('',(0.500000000000009,0.,-0.866025403784434));
#7318=DIRECTION('',(0.,-1.,0.));
#7319=DIRECTION('',(0.,0.,-1.));
#7320=DIRECTION('',(0.,-1.,0.));
#7321=DIRECTION('',(0.,0.,-1.));
#7322=DIRECTION('',(0.,-1.,0.));
#7323=DIRECTION('',(0.,0.,-1.));
#7324=DIRECTION('',(0.500000000000008,0.,-0.866025403784434));
#7325=DIRECTION('',(-0.866025403784434,0.,-0.500000000000009));
#7326=DIRECTION('',(0.866025403784434,0.,0.500000000000009));
#7327=DIRECTION('',(0.866025403784434,0.,0.500000000000009));
#7328=DIRECTION('',(0.,-1.,0.));
#7329=DIRECTION('',(0.,0.,-1.));
#7330=DIRECTION('',(0.,-1.,0.));
#7331=DIRECTION('',(0.,0.,-1.));
#7332=DIRECTION('',(0.,-1.,0.));
#7333=DIRECTION('',(0.,0.,-1.));
#7334=DIRECTION('',(0.,-1.,0.));
#7335=DIRECTION('',(0.,0.,-1.));
#7336=DIRECTION('',(0.,-1.,0.));
#7337=DIRECTION('',(0.,0.,-1.));
#7338=DIRECTION('',(0.,-1.,0.));
#7339=DIRECTION('',(0.,0.,-1.));
#7340=DIRECTION('',(0.,-1.,0.));
#7341=DIRECTION('',(0.,0.,-1.));
#7342=DIRECTION('',(0.,-1.,0.));
#7343=DIRECTION('',(0.,0.,-1.));
#7344=DIRECTION('',(0.,-1.,0.));
#7345=DIRECTION('',(0.,0.,-1.));
#7346=DIRECTION('',(0.,-1.,0.));
#7347=DIRECTION('',(0.,0.,-1.));
#7348=DIRECTION('',(0.,-1.,0.));
#7349=DIRECTION('',(0.,0.,-1.));
#7350=DIRECTION('',(0.,-1.,0.));
#7351=DIRECTION('',(0.,0.,-1.));
#7352=DIRECTION('',(0.,-1.,0.));
#7353=DIRECTION('',(0.,0.,-1.));
#7354=DIRECTION('',(0.,-1.,0.));
#7355=DIRECTION('',(0.,0.,-1.));
#7356=DIRECTION('',(0.,-1.,0.));
#7357=DIRECTION('',(0.,0.,-1.));
#7358=DIRECTION('',(0.,-1.,0.));
#7359=DIRECTION('',(0.,0.,-1.));
#7360=DIRECTION('',(0.,1.,0.));
#7361=DIRECTION('',(0.,0.,1.));
#8391=CARTESIAN_POINT('',(0.,0.,0.));
#9154=CARTESIAN_POINT('',(-0.00370266623767647,-0.0055,-0.00213773534904185));
#9155=CARTESIAN_POINT('',(-0.00370266623767647,-0.0065,-0.00213773534904185));
#9156=CARTESIAN_POINT('',(-0.0074173999821892,-0.0065,0.00429637223304478));
#9157=CARTESIAN_POINT('',(-2.42942346645285E-5,-0.0065,-0.00850886254739745));
#9158=CARTESIAN_POINT('',(-0.0074173999821892,-0.0055,0.00429637223304478));
#9159=CARTESIAN_POINT('',(-0.0074173999821892,-0.0055,0.00429637223304478));
#9160=CARTESIAN_POINT('',(-0.00370266623767647,-0.0055,-0.00213773534904185));
#9161=CARTESIAN_POINT('',(-2.42942346645285E-5,-0.0055,-0.00850886254739745));
#9162=CARTESIAN_POINT('',(-2.42942346645285E-5,-0.0055,-0.00850886254739745));
#9163=CARTESIAN_POINT('',(-0.00371473374451272,-0.0055,0.00643410758208663));
#9164=CARTESIAN_POINT('',(-0.00371473374451272,-0.0065,0.00643410758208663));
#9165=CARTESIAN_POINT('',(0.015179183486316,-0.0065,0.0173425157813521));
#9166=CARTESIAN_POINT('',(0.015179183486316,-0.0055,0.0173425157813521));
#9167=CARTESIAN_POINT('',(0.015179183486316,-0.0055,0.0173425157813521));
#9168=CARTESIAN_POINT('',(-0.00371473374451272,-0.0055,0.00643410758208663));
#9169=CARTESIAN_POINT('',(0.0188939172308287,-0.0055,0.0109084081992657));
#9170=CARTESIAN_POINT('',(0.0188939172308287,-0.0065,0.0109084081992657));
#9171=CARTESIAN_POINT('',(0.0225722892338407,-0.0065,0.00453728100091018));
#9172=CARTESIAN_POINT('',(0.0225722892338407,-0.0055,0.00453728100091018));
#9173=CARTESIAN_POINT('',(0.0225722892338407,-0.0055,0.00453728100091018));
#9174=CARTESIAN_POINT('',(0.0188939172308287,-0.0055,0.0109084081992657));
#9175=CARTESIAN_POINT('',(-0.00266693662555068,-0.0055,0.00406832833985245));
#9176=CARTESIAN_POINT('',(-0.00266693662555068,-0.0055,0.00406832833985245));
#9177=CARTESIAN_POINT('',(-0.00266693662555068,-0.0055,0.00256832833985245));
#9178=CARTESIAN_POINT('',(-0.00266693662555068,-0.0065,0.00406832833985245));
#9179=CARTESIAN_POINT('',(-0.00266693662555068,-0.0065,0.00256832833985245));
#9180=CARTESIAN_POINT('',(0.00367837200301199,-0.0055,-0.00637112719835552));
#9181=CARTESIAN_POINT('',(0.00367837200301199,-0.0065,-0.00637112719835552));
#9182=CARTESIAN_POINT('',(0.00367837200301199,-0.0055,-0.00637112719835552));
#9183=CARTESIAN_POINT('',(0.0151554445662277,-0.0055,0.00875));
#9184=CARTESIAN_POINT('',(0.0151554445662277,-0.0055,0.00875));
#9185=CARTESIAN_POINT('',(0.0151554445662277,-0.0055,0.00725));
#9186=CARTESIAN_POINT('',(0.0151554445662277,-0.0065,0.00875));
#9187=CARTESIAN_POINT('',(0.0151554445662277,-0.0065,0.00725));
#9188=CARTESIAN_POINT('',(0.0178581876187029,-0.0055,0.00470234451037119));
#9189=CARTESIAN_POINT('',(0.0178581876187029,-0.0055,0.00470234451037119));
#9190=CARTESIAN_POINT('',(0.0178581876187029,-0.0055,0.00320234451037119));
#9191=CARTESIAN_POINT('',(0.0178581876187029,-0.0065,0.00470234451037119));
#9192=CARTESIAN_POINT('',(0.0178581876187029,-0.0065,0.00320234451037119));
#9193=CARTESIAN_POINT('',(0.00218980738047307,-0.0055,-0.00434379903793625));
#9194=CARTESIAN_POINT('',(0.00218980738047307,-0.0055,-0.00434379903793625));
#9195=CARTESIAN_POINT('',(0.00218980738047307,-0.0055,-0.00584379903793625));
#9196=CARTESIAN_POINT('',(0.00218980738047307,-0.0065,-0.00434379903793625));
#9197=CARTESIAN_POINT('',(0.00218980738047307,-0.0065,-0.00584379903793625));
#9198=CARTESIAN_POINT('',(0.0130014436126792,-0.0055,0.0131144718881599));
#9199=CARTESIAN_POINT('',(0.0130014436126792,-0.0055,0.0131144718881599));
#9200=CARTESIAN_POINT('',(0.0130014436126792,-0.0055,0.0116144718881599));
#9201=CARTESIAN_POINT('',(0.0130014436126792,-0.0065,0.0131144718881599));
#9202=CARTESIAN_POINT('',(0.0130014436126792,-0.0065,0.0116144718881599));
#9203=CARTESIAN_POINT('',(0.,-0.0055,0.));
#9204=CARTESIAN_POINT('',(0.,-0.0055,0.));
#9205=CARTESIAN_POINT('',(0.,-0.0055,-0.0015));
#9206=CARTESIAN_POINT('',(0.,-0.0065,0.));
#9207=CARTESIAN_POINT('',(0.,-0.0065,0.));
#9208=CARTESIAN_POINT('',(0.,-0.0065,-0.0015));
#9209=CARTESIAN_POINT('',(0.,-0.0105,0.));
#10141=MECHANICAL_DESIGN_GEOMETRIC_PRESENTATION_REPRESENTATION('',(#5558),#10142);
#10142=(
GEOMETRIC_REPRESENTATION_CONTEXT(3)
GLOBAL_UNCERTAINTY_ASSIGNED_CONTEXT((#10158))
GLOBAL_UNIT_ASSIGNED_CONTEXT((#10176,#10175,#10174))
REPRESENTATION_CONTEXT('MAS-674','TOP_LEVEL_ASSEMBLY_PART')
);
#10148=(
GEOMETRIC_REPRESENTATION_CONTEXT(3)
GLOBAL_UNCERTAINTY_ASSIGNED_CONTEXT((#10164))
GLOBAL_UNIT_ASSIGNED_CONTEXT((#10176,#10175,#10174))
REPRESENTATION_CONTEXT('Part 2','COMPONENT_PART')
);
#10158=UNCERTAINTY_MEASURE_WITH_UNIT(LENGTH_MEASURE(1.E-8),#10176,
'DISTANCE_ACCURACY_VALUE','Maximum Tolerance applied to model');
#10164=UNCERTAINTY_MEASURE_WITH_UNIT(LENGTH_MEASURE(1.E-8),#10176,
'DISTANCE_ACCURACY_VALUE','Maximum Tolerance applied to model');
#10174=(
NAMED_UNIT(*)
SI_UNIT($,.STERADIAN.)
SOLID_ANGLE_UNIT()
);
#10175=(
NAMED_UNIT(*)
PLANE_ANGLE_UNIT()
SI_UNIT($,.RADIAN.)
);
#10176=(
LENGTH_UNIT()
NAMED_UNIT(*)
SI_UNIT($,.METRE.)
);
#10190=PRODUCT_DEFINITION_SHAPE('','',#10216);
#10216=PRODUCT_DEFINITION('','',#10248,#10232);
#10232=PRODUCT_DEFINITION_CONTEXT('',#10323,'design');
#10248=PRODUCT_DEFINITION_FORMATION_WITH_SPECIFIED_SOURCE('','',#10280,
 .NOT_KNOWN.);
#10280=PRODUCT('Part 2','Part 2','Part 2',(#10312));
#10312=PRODUCT_CONTEXT('',#10323,'mechanical');
#10323=APPLICATION_CONTEXT('managed model based 3d engineering');
ENDSEC;
END-ISO-10303-21;
